ISO-10303-21;
HEADER;
/* Generated by software containing ST-Developer
 * from STEP Tools, Inc. (www.steptools.com) 
 */

FILE_DESCRIPTION(
/* description */ ('Bell-crank linkage with push rods'),
/* implementation_level */ '2;1');

FILE_NAME(
/* name */ 'Pin keeper (2).step',
/* time_stamp */ '2026-10-28T03:25:15-07:00',
/* author */ (''),
/* organization */ (''),
/* preprocessor_version */ 'ST-DEVELOPER v20.2',
/* originating_system */ 'Autodesk Translation Framework v15.17.0.0',
/* authorisation */ '');

FILE_SCHEMA (('AUTOMOTIVE_DESIGN { 1 0 10303 214 3 1 1 }'));
ENDSEC;

DATA;
#10=MECHANICAL_DESIGN_GEOMETRIC_PRESENTATION_REPRESENTATION('',(#655),#16678);
#539=SHAPE_REPRESENTATION_RELATIONSHIP('SRR','None',#16960,#593);
#593=ADVANCED_BREP_SHAPE_REPRESENTATION('',(#715),#16665);
#655=STYLED_ITEM('',(#17291),#715);
#715=MANIFOLD_SOLID_BREP('Body1',#8847);
#912=FACE_BOUND('',#2380,.T.);
#913=FACE_BOUND('',#2382,.T.);
#1187=PLANE('',#10348);
#1188=PLANE('',#10349);
#1668=FACE_OUTER_BOUND('',#2377,.T.);
#1669=FACE_OUTER_BOUND('',#2378,.T.);
#1670=FACE_OUTER_BOUND('',#2379,.T.);
#1671=FACE_OUTER_BOUND('',#2381,.T.);
#2377=EDGE_LOOP('',(#7671,#7672,#7673,#7674));
#2378=EDGE_LOOP('',(#7675,#7676,#7677,#7678));
#2379=EDGE_LOOP('',(#7679));
#2380=EDGE_LOOP('',(#7680));
#2381=EDGE_LOOP('',(#7681));
#2382=EDGE_LOOP('',(#7682));
#2968=LINE('',#16023,#3517);
#2969=LINE('',#16029,#3518);
#3517=VECTOR('',#12846,0.225);
#3518=VECTOR('',#12853,0.5);
#4035=CIRCLE('',#10343,0.225);
#4036=CIRCLE('',#10344,0.225);
#4037=CIRCLE('',#10346,0.5);
#4038=CIRCLE('',#10347,0.5);
#4702=VERTEX_POINT('',#16020);
#4703=VERTEX_POINT('',#16022);
#4704=VERTEX_POINT('',#16026);
#4705=VERTEX_POINT('',#16028);
#5713=EDGE_CURVE('',#4702,#4702,#4035,.T.);
#5714=EDGE_CURVE('',#4702,#4703,#2968,.T.);
#5715=EDGE_CURVE('',#4703,#4703,#4036,.T.);
#5716=EDGE_CURVE('',#4704,#4704,#4037,.T.);
#5717=EDGE_CURVE('',#4704,#4705,#2969,.T.);
#5718=EDGE_CURVE('',#4705,#4705,#4038,.T.);
#7671=ORIENTED_EDGE('',*,*,#5713,.F.);
#7672=ORIENTED_EDGE('',*,*,#5714,.T.);
#7673=ORIENTED_EDGE('',*,*,#5715,.T.);
#7674=ORIENTED_EDGE('',*,*,#5714,.F.);
#7675=ORIENTED_EDGE('',*,*,#5716,.F.);
#7676=ORIENTED_EDGE('',*,*,#5717,.T.);
#7677=ORIENTED_EDGE('',*,*,#5718,.T.);
#7678=ORIENTED_EDGE('',*,*,#5717,.F.);
#7679=ORIENTED_EDGE('',*,*,#5716,.T.);
#7680=ORIENTED_EDGE('',*,*,#5713,.T.);
#7681=ORIENTED_EDGE('',*,*,#5718,.F.);
#7682=ORIENTED_EDGE('',*,*,#5715,.F.);
#8234=CYLINDRICAL_SURFACE('',#10342,0.225);
#8235=CYLINDRICAL_SURFACE('',#10345,0.5);
#8693=ADVANCED_FACE('',(#1668),#8234,.F.);
#8694=ADVANCED_FACE('',(#1669),#8235,.T.);
#8695=ADVANCED_FACE('',(#1670,#912),#1187,.T.);
#8696=ADVANCED_FACE('',(#1671,#913),#1188,.F.);
#8847=CLOSED_SHELL('',(#8693,#8694,#8695,#8696));
#10341=AXIS2_PLACEMENT_3D('',#16018,#12840,#12841);
#10342=AXIS2_PLACEMENT_3D('',#16019,#12842,#12843);
#10343=AXIS2_PLACEMENT_3D('',#16021,#12844,#12845);
#10344=AXIS2_PLACEMENT_3D('',#16024,#12847,#12848);
#10345=AXIS2_PLACEMENT_3D('',#16025,#12849,#12850);
#10346=AXIS2_PLACEMENT_3D('',#16027,#12851,#12852);
#10347=AXIS2_PLACEMENT_3D('',#16030,#12854,#12855);
#10348=AXIS2_PLACEMENT_3D('',#16031,#12856,#12857);
#10349=AXIS2_PLACEMENT_3D('',#16032,#12858,#12859);
#12840=DIRECTION('axis',(0.,0.,1.));
#12841=DIRECTION('refdir',(1.,0.,0.));
#12842=DIRECTION('center_axis',(0.,0.,1.));
#12843=DIRECTION('ref_axis',(1.,0.,0.));
#12844=DIRECTION('center_axis',(0.,0.,-1.));
#12845=DIRECTION('ref_axis',(1.,0.,0.));
#12846=DIRECTION('',(0.,0.,-1.));
#12847=DIRECTION('center_axis',(0.,0.,-1.));
#12848=DIRECTION('ref_axis',(1.,0.,0.));
#12849=DIRECTION('center_axis',(0.,0.,1.));
#12850=DIRECTION('ref_axis',(1.,0.,0.));
#12851=DIRECTION('center_axis',(0.,0.,1.));
#12852=DIRECTION('ref_axis',(1.,0.,0.));
#12853=DIRECTION('',(0.,0.,-1.));
#12854=DIRECTION('center_axis',(0.,0.,1.));
#12855=DIRECTION('ref_axis',(1.,0.,0.));
#12856=DIRECTION('center_axis',(0.,0.,1.));
#12857=DIRECTION('ref_axis',(1.,0.,0.));
#12858=DIRECTION('center_axis',(0.,0.,1.));
#12859=DIRECTION('ref_axis',(1.,0.,0.));
#16018=CARTESIAN_POINT('',(0.,0.,0.));
#16019=CARTESIAN_POINT('Origin',(10.,2.,10.1));
#16020=CARTESIAN_POINT('',(9.775,2.,10.3));
#16021=CARTESIAN_POINT('Origin',(10.,2.,10.3));
#16022=CARTESIAN_POINT('',(9.775,2.,10.1));
#16023=CARTESIAN_POINT('',(9.775,2.,10.1));
#16024=CARTESIAN_POINT('Origin',(10.,2.,10.1));
#16025=CARTESIAN_POINT('Origin',(10.,2.,10.1));
#16026=CARTESIAN_POINT('',(9.5,2.,10.3));
#16027=CARTESIAN_POINT('Origin',(10.,2.,10.3));
#16028=CARTESIAN_POINT('',(9.5,2.,10.1));
#16029=CARTESIAN_POINT('',(9.5,2.,10.1));
#16030=CARTESIAN_POINT('Origin',(10.,2.,10.1));
#16031=CARTESIAN_POINT('Origin',(10.,2.,10.3));
#16032=CARTESIAN_POINT('Origin',(10.,2.,10.1));
#16601=UNCERTAINTY_MEASURE_WITH_UNIT(LENGTH_MEASURE(0.001),#16679,
'DISTANCE_ACCURACY_VALUE',
'Maximum model space distance between geometric entities at asserted c
onnectivities');
#16614=UNCERTAINTY_MEASURE_WITH_UNIT(LENGTH_MEASURE(0.001),#16679,
'DISTANCE_ACCURACY_VALUE',
'Maximum model space distance between geometric entities at asserted c
onnectivities');
#16665=(
GEOMETRIC_REPRESENTATION_CONTEXT(3)
GLOBAL_UNCERTAINTY_ASSIGNED_CONTEXT((#16601))
GLOBAL_UNIT_ASSIGNED_CONTEXT((#16679,#16681,#16682))
REPRESENTATION_CONTEXT('','3D')
);
#16678=(
GEOMETRIC_REPRESENTATION_CONTEXT(3)
GLOBAL_UNCERTAINTY_ASSIGNED_CONTEXT((#16614))
GLOBAL_UNIT_ASSIGNED_CONTEXT((#16679,#16681,#16682))
REPRESENTATION_CONTEXT('','3D')
);
#16679=(
LENGTH_UNIT()
NAMED_UNIT(*)
SI_UNIT(.CENTI.,.METRE.)
);
#16681=(
NAMED_UNIT(*)
PLANE_ANGLE_UNIT()
SI_UNIT($,.RADIAN.)
);
#16682=(
NAMED_UNIT(*)
SI_UNIT($,.STERADIAN.)
SOLID_ANGLE_UNIT()
);
#16733=SHAPE_DEFINITION_REPRESENTATION(#16807,#16960);
#16807=PRODUCT_DEFINITION_SHAPE('',$,#17024);
#16960=SHAPE_REPRESENTATION('',(#10341),#16665);
#16973=PRODUCT_DEFINITION_CONTEXT('part definition',#17164,'design');
#17024=PRODUCT_DEFINITION('Pin keeper (2)','Pin keeper (2)',#17087,#16973);
#17087=PRODUCT_DEFINITION_FORMATION('',$,#17216);
#17164=APPLICATION_CONTEXT(
'Core Data for Automotive Mechanical Design Process');
#17165=PRODUCT_CONTEXT('part definition',#17164,'mechanical');
#17216=PRODUCT('Pin keeper (2)','Pin keeper (2)','Pin keeper (2)',(#17165));
#17285=COLOUR_RGB('Grey',0.48,0.52,0.57);
#17286=FILL_AREA_STYLE_COLOUR('',#17285);
#17287=FILL_AREA_STYLE('',(#17286));
#17288=SURFACE_STYLE_FILL_AREA(#17287);
#17289=SURFACE_SIDE_STYLE('',(#17288));
#17290=SURFACE_STYLE_USAGE(.BOTH.,#17289);
#17291=PRESENTATION_STYLE_ASSIGNMENT((#17290));
ENDSEC;
END-ISO-10303-21;
